ISO-10303-21;
HEADER;
/* Generated by software containing ST-Developer
 * from STEP Tools, Inc. (www.steptools.com) 
 */

FILE_DESCRIPTION(
/* description */ (''),
/* implementation_level */ '2;1');

FILE_NAME(
/* name */ 'Screw_03.step',
/* time_stamp */ '2026-10-06T13:23:02-07:00',
/* author */ (''),
/* organization */ (''),
/* preprocessor_version */ 'ST-DEVELOPER v20.2',
/* originating_system */ 'Autodesk Translation Framework v15.15.0.0',
/* authorisation */ '');

FILE_SCHEMA (('AUTOMOTIVE_DESIGN { 1 0 10303 214 3 1 1 }'));
ENDSEC;

DATA;
#10=MECHANICAL_DESIGN_GEOMETRIC_PRESENTATION_REPRESENTATION('',(#73),#4994);
#53=SHAPE_REPRESENTATION_RELATIONSHIP('SRR','None',#5034,#63);
#63=ADVANCED_BREP_SHAPE_REPRESENTATION('',(#83),#4986);
#73=STYLED_ITEM('',(#5091),#83);
#83=MANIFOLD_SOLID_BREP('Body1',#2913);
#95=CYLINDRICAL_SURFACE('',#3096,1.9);
#96=CYLINDRICAL_SURFACE('',#3110,0.96675);
#127=FACE_BOUND('',#526,.T.);
#128=FACE_BOUND('',#543,.T.);
#196=PLANE('',#3095);
#197=PLANE('',#3098);
#198=PLANE('',#3099);
#199=PLANE('',#3100);
#200=PLANE('',#3101);
#201=PLANE('',#3102);
#202=PLANE('',#3103);
#203=PLANE('',#3104);
#204=PLANE('',#3105);
#205=PLANE('',#3106);
#206=PLANE('',#3107);
#207=PLANE('',#3108);
#208=PLANE('',#3109);
#209=PLANE('',#3112);
#210=PLANE('',#3113);
#301=TOROIDAL_SURFACE('',#3091,1.7,0.2);
#341=FACE_OUTER_BOUND('',#523,.T.);
#342=FACE_OUTER_BOUND('',#524,.T.);
#343=FACE_OUTER_BOUND('',#525,.T.);
#344=FACE_OUTER_BOUND('',#527,.T.);
#345=FACE_OUTER_BOUND('',#528,.T.);
#346=FACE_OUTER_BOUND('',#529,.T.);
#347=FACE_OUTER_BOUND('',#530,.T.);
#348=FACE_OUTER_BOUND('',#531,.T.);
#349=FACE_OUTER_BOUND('',#532,.T.);
#350=FACE_OUTER_BOUND('',#533,.T.);
#351=FACE_OUTER_BOUND('',#534,.T.);
#352=FACE_OUTER_BOUND('',#535,.T.);
#353=FACE_OUTER_BOUND('',#536,.T.);
#354=FACE_OUTER_BOUND('',#537,.T.);
#355=FACE_OUTER_BOUND('',#538,.T.);
#356=FACE_OUTER_BOUND('',#539,.T.);
#357=FACE_OUTER_BOUND('',#540,.T.);
#358=FACE_OUTER_BOUND('',#541,.T.);
#359=FACE_OUTER_BOUND('',#542,.T.);
#523=EDGE_LOOP('',(#2112,#2113,#2114,#2115));
#524=EDGE_LOOP('',(#2116,#2117,#2118,#2119));
#525=EDGE_LOOP('',(#2120));
#526=EDGE_LOOP('',(#2121,#2122,#2123,#2124,#2125,#2126));
#527=EDGE_LOOP('',(#2127,#2128,#2129,#2130));
#528=EDGE_LOOP('',(#2131,#2132,#2133));
#529=EDGE_LOOP('',(#2134,#2135,#2136));
#530=EDGE_LOOP('',(#2137,#2138,#2139));
#531=EDGE_LOOP('',(#2140,#2141,#2142));
#532=EDGE_LOOP('',(#2143,#2144,#2145));
#533=EDGE_LOOP('',(#2146,#2147,#2148));
#534=EDGE_LOOP('',(#2149,#2150,#2151,#2152));
#535=EDGE_LOOP('',(#2153,#2154,#2155,#2156));
#536=EDGE_LOOP('',(#2157,#2158,#2159,#2160));
#537=EDGE_LOOP('',(#2161,#2162,#2163,#2164));
#538=EDGE_LOOP('',(#2165,#2166,#2167,#2168));
#539=EDGE_LOOP('',(#2169,#2170,#2171,#2172));
#540=EDGE_LOOP('',(#2173,#2174,#2175,#2176));
#541=EDGE_LOOP('',(#2177));
#542=EDGE_LOOP('',(#2178));
#543=EDGE_LOOP('',(#2179));
#756=LINE('',#4317,#1049);
#757=LINE('',#4328,#1050);
#758=LINE('',#4330,#1051);
#759=LINE('',#4332,#1052);
#760=LINE('',#4334,#1053);
#761=LINE('',#4336,#1054);
#762=LINE('',#4337,#1055);
#763=LINE('',#4341,#1056);
#764=LINE('',#4345,#1057);
#765=LINE('',#4347,#1058);
#766=LINE('',#4348,#1059);
#767=LINE('',#4351,#1060);
#768=LINE('',#4352,#1061);
#769=LINE('',#4355,#1062);
#770=LINE('',#4356,#1063);
#771=LINE('',#4359,#1064);
#772=LINE('',#4360,#1065);
#773=LINE('',#4363,#1066);
#774=LINE('',#4364,#1067);
#775=LINE('',#4366,#1068);
#776=LINE('',#4368,#1069);
#777=LINE('',#4369,#1070);
#778=LINE('',#4371,#1071);
#779=LINE('',#4373,#1072);
#780=LINE('',#4375,#1073);
#781=LINE('',#4377,#1074);
#782=LINE('',#4381,#1075);
#1049=VECTOR('',#3482,0.887310000000001);
#1050=VECTOR('',#3495,10.);
#1051=VECTOR('',#3496,10.);
#1052=VECTOR('',#3497,10.);
#1053=VECTOR('',#3498,10.);
#1054=VECTOR('',#3499,10.);
#1055=VECTOR('',#3500,10.);
#1056=VECTOR('',#3505,1.9);
#1057=VECTOR('',#3508,9.99999999999999);
#1058=VECTOR('',#3509,10.);
#1059=VECTOR('',#3510,10.);
#1060=VECTOR('',#3513,10.);
#1061=VECTOR('',#3514,10.);
#1062=VECTOR('',#3517,10.);
#1063=VECTOR('',#3518,9.99999999999999);
#1064=VECTOR('',#3521,10.);
#1065=VECTOR('',#3522,10.);
#1066=VECTOR('',#3525,10.);
#1067=VECTOR('',#3526,10.);
#1068=VECTOR('',#3529,10.);
#1069=VECTOR('',#3532,10.);
#1070=VECTOR('',#3533,10.);
#1071=VECTOR('',#3536,10.);
#1072=VECTOR('',#3539,10.);
#1073=VECTOR('',#3542,10.);
#1074=VECTOR('',#3545,10.);
#1075=VECTOR('',#3550,0.96675);
#1302=CIRCLE('',#3089,0.96675);
#1303=CIRCLE('',#3090,0.754619999999998);
#1304=CIRCLE('',#3092,1.9);
#1305=CIRCLE('',#3093,0.2);
#1306=CIRCLE('',#3094,1.7);
#1307=CIRCLE('',#3097,1.9);
#1308=CIRCLE('',#3111,0.96675);
#1407=VERTEX_POINT('',#4314);
#1408=VERTEX_POINT('',#4316);
#1409=VERTEX_POINT('',#4320);
#1410=VERTEX_POINT('',#4322);
#1411=VERTEX_POINT('',#4326);
#1412=VERTEX_POINT('',#4327);
#1413=VERTEX_POINT('',#4329);
#1414=VERTEX_POINT('',#4331);
#1415=VERTEX_POINT('',#4333);
#1416=VERTEX_POINT('',#4335);
#1417=VERTEX_POINT('',#4339);
#1418=VERTEX_POINT('',#4343);
#1419=VERTEX_POINT('',#4344);
#1420=VERTEX_POINT('',#4346);
#1421=VERTEX_POINT('',#4350);
#1422=VERTEX_POINT('',#4354);
#1423=VERTEX_POINT('',#4358);
#1424=VERTEX_POINT('',#4362);
#1425=VERTEX_POINT('',#4380);
#1670=EDGE_CURVE('',#1407,#1407,#1302,.T.);
#1671=EDGE_CURVE('',#1407,#1408,#756,.T.);
#1672=EDGE_CURVE('',#1408,#1408,#1303,.T.);
#1673=EDGE_CURVE('',#1409,#1409,#1304,.T.);
#1674=EDGE_CURVE('',#1409,#1410,#1305,.T.);
#1675=EDGE_CURVE('',#1410,#1410,#1306,.T.);
#1676=EDGE_CURVE('',#1411,#1412,#757,.T.);
#1677=EDGE_CURVE('',#1412,#1413,#758,.T.);
#1678=EDGE_CURVE('',#1413,#1414,#759,.T.);
#1679=EDGE_CURVE('',#1414,#1415,#760,.T.);
#1680=EDGE_CURVE('',#1415,#1416,#761,.T.);
#1681=EDGE_CURVE('',#1416,#1411,#762,.T.);
#1682=EDGE_CURVE('',#1417,#1417,#1307,.T.);
#1683=EDGE_CURVE('',#1417,#1409,#763,.T.);
#1684=EDGE_CURVE('',#1418,#1419,#764,.T.);
#1685=EDGE_CURVE('',#1420,#1418,#765,.T.);
#1686=EDGE_CURVE('',#1420,#1419,#766,.T.);
#1687=EDGE_CURVE('',#1421,#1420,#767,.T.);
#1688=EDGE_CURVE('',#1421,#1419,#768,.T.);
#1689=EDGE_CURVE('',#1422,#1421,#769,.T.);
#1690=EDGE_CURVE('',#1422,#1419,#770,.T.);
#1691=EDGE_CURVE('',#1423,#1422,#771,.T.);
#1692=EDGE_CURVE('',#1423,#1419,#772,.T.);
#1693=EDGE_CURVE('',#1424,#1423,#773,.T.);
#1694=EDGE_CURVE('',#1424,#1419,#774,.T.);
#1695=EDGE_CURVE('',#1418,#1424,#775,.T.);
#1696=EDGE_CURVE('',#1411,#1420,#776,.T.);
#1697=EDGE_CURVE('',#1412,#1418,#777,.T.);
#1698=EDGE_CURVE('',#1416,#1421,#778,.T.);
#1699=EDGE_CURVE('',#1415,#1422,#779,.T.);
#1700=EDGE_CURVE('',#1414,#1423,#780,.T.);
#1701=EDGE_CURVE('',#1413,#1424,#781,.T.);
#1702=EDGE_CURVE('',#1407,#1425,#782,.T.);
#1703=EDGE_CURVE('',#1425,#1425,#1308,.F.);
#2112=ORIENTED_EDGE('',*,*,#1670,.F.);
#2113=ORIENTED_EDGE('',*,*,#1671,.T.);
#2114=ORIENTED_EDGE('',*,*,#1672,.F.);
#2115=ORIENTED_EDGE('',*,*,#1671,.F.);
#2116=ORIENTED_EDGE('',*,*,#1673,.T.);
#2117=ORIENTED_EDGE('',*,*,#1674,.T.);
#2118=ORIENTED_EDGE('',*,*,#1675,.T.);
#2119=ORIENTED_EDGE('',*,*,#1674,.F.);
#2120=ORIENTED_EDGE('',*,*,#1675,.F.);
#2121=ORIENTED_EDGE('',*,*,#1676,.T.);
#2122=ORIENTED_EDGE('',*,*,#1677,.T.);
#2123=ORIENTED_EDGE('',*,*,#1678,.T.);
#2124=ORIENTED_EDGE('',*,*,#1679,.T.);
#2125=ORIENTED_EDGE('',*,*,#1680,.T.);
#2126=ORIENTED_EDGE('',*,*,#1681,.T.);
#2127=ORIENTED_EDGE('',*,*,#1682,.F.);
#2128=ORIENTED_EDGE('',*,*,#1683,.T.);
#2129=ORIENTED_EDGE('',*,*,#1673,.F.);
#2130=ORIENTED_EDGE('',*,*,#1683,.F.);
#2131=ORIENTED_EDGE('',*,*,#1684,.F.);
#2132=ORIENTED_EDGE('',*,*,#1685,.F.);
#2133=ORIENTED_EDGE('',*,*,#1686,.T.);
#2134=ORIENTED_EDGE('',*,*,#1686,.F.);
#2135=ORIENTED_EDGE('',*,*,#1687,.F.);
#2136=ORIENTED_EDGE('',*,*,#1688,.T.);
#2137=ORIENTED_EDGE('',*,*,#1688,.F.);
#2138=ORIENTED_EDGE('',*,*,#1689,.F.);
#2139=ORIENTED_EDGE('',*,*,#1690,.T.);
#2140=ORIENTED_EDGE('',*,*,#1690,.F.);
#2141=ORIENTED_EDGE('',*,*,#1691,.F.);
#2142=ORIENTED_EDGE('',*,*,#1692,.T.);
#2143=ORIENTED_EDGE('',*,*,#1692,.F.);
#2144=ORIENTED_EDGE('',*,*,#1693,.F.);
#2145=ORIENTED_EDGE('',*,*,#1694,.T.);
#2146=ORIENTED_EDGE('',*,*,#1694,.F.);
#2147=ORIENTED_EDGE('',*,*,#1695,.F.);
#2148=ORIENTED_EDGE('',*,*,#1684,.T.);
#2149=ORIENTED_EDGE('',*,*,#1676,.F.);
#2150=ORIENTED_EDGE('',*,*,#1696,.T.);
#2151=ORIENTED_EDGE('',*,*,#1685,.T.);
#2152=ORIENTED_EDGE('',*,*,#1697,.F.);
#2153=ORIENTED_EDGE('',*,*,#1681,.F.);
#2154=ORIENTED_EDGE('',*,*,#1698,.T.);
#2155=ORIENTED_EDGE('',*,*,#1687,.T.);
#2156=ORIENTED_EDGE('',*,*,#1696,.F.);
#2157=ORIENTED_EDGE('',*,*,#1680,.F.);
#2158=ORIENTED_EDGE('',*,*,#1699,.T.);
#2159=ORIENTED_EDGE('',*,*,#1689,.T.);
#2160=ORIENTED_EDGE('',*,*,#1698,.F.);
#2161=ORIENTED_EDGE('',*,*,#1679,.F.);
#2162=ORIENTED_EDGE('',*,*,#1700,.T.);
#2163=ORIENTED_EDGE('',*,*,#1691,.T.);
#2164=ORIENTED_EDGE('',*,*,#1699,.F.);
#2165=ORIENTED_EDGE('',*,*,#1678,.F.);
#2166=ORIENTED_EDGE('',*,*,#1701,.T.);
#2167=ORIENTED_EDGE('',*,*,#1693,.T.);
#2168=ORIENTED_EDGE('',*,*,#1700,.F.);
#2169=ORIENTED_EDGE('',*,*,#1677,.F.);
#2170=ORIENTED_EDGE('',*,*,#1697,.T.);
#2171=ORIENTED_EDGE('',*,*,#1695,.T.);
#2172=ORIENTED_EDGE('',*,*,#1701,.F.);
#2173=ORIENTED_EDGE('',*,*,#1670,.T.);
#2174=ORIENTED_EDGE('',*,*,#1702,.T.);
#2175=ORIENTED_EDGE('',*,*,#1703,.T.);
#2176=ORIENTED_EDGE('',*,*,#1702,.F.);
#2177=ORIENTED_EDGE('',*,*,#1672,.T.);
#2178=ORIENTED_EDGE('',*,*,#1682,.T.);
#2179=ORIENTED_EDGE('',*,*,#1703,.F.);
#2726=CONICAL_SURFACE('',#3088,0.887310000000001,0.824535502685815);
#2771=ADVANCED_FACE('',(#341),#2726,.T.);
#2772=ADVANCED_FACE('',(#342),#301,.T.);
#2773=ADVANCED_FACE('',(#343,#127),#196,.T.);
#2774=ADVANCED_FACE('',(#344),#95,.T.);
#2775=ADVANCED_FACE('',(#345),#197,.F.);
#2776=ADVANCED_FACE('',(#346),#198,.F.);
#2777=ADVANCED_FACE('',(#347),#199,.F.);
#2778=ADVANCED_FACE('',(#348),#200,.F.);
#2779=ADVANCED_FACE('',(#349),#201,.F.);
#2780=ADVANCED_FACE('',(#350),#202,.F.);
#2781=ADVANCED_FACE('',(#351),#203,.F.);
#2782=ADVANCED_FACE('',(#352),#204,.F.);
#2783=ADVANCED_FACE('',(#353),#205,.F.);
#2784=ADVANCED_FACE('',(#354),#206,.F.);
#2785=ADVANCED_FACE('',(#355),#207,.F.);
#2786=ADVANCED_FACE('',(#356),#208,.F.);
#2787=ADVANCED_FACE('',(#357),#96,.T.);
#2788=ADVANCED_FACE('',(#358),#209,.T.);
#2789=ADVANCED_FACE('',(#359,#128),#210,.T.);
#2913=CLOSED_SHELL('',(#2771,#2772,#2773,#2774,#2775,#2776,#2777,#2778,
#2779,#2780,#2781,#2782,#2783,#2784,#2785,#2786,#2787,#2788,#2789));
#3087=AXIS2_PLACEMENT_3D('',#4312,#3476,#3477);
#3088=AXIS2_PLACEMENT_3D('',#4313,#3478,#3479);
#3089=AXIS2_PLACEMENT_3D('',#4315,#3480,#3481);
#3090=AXIS2_PLACEMENT_3D('',#4318,#3483,#3484);
#3091=AXIS2_PLACEMENT_3D('',#4319,#3485,#3486);
#3092=AXIS2_PLACEMENT_3D('',#4321,#3487,#3488);
#3093=AXIS2_PLACEMENT_3D('',#4323,#3489,#3490);
#3094=AXIS2_PLACEMENT_3D('',#4324,#3491,#3492);
#3095=AXIS2_PLACEMENT_3D('',#4325,#3493,#3494);
#3096=AXIS2_PLACEMENT_3D('',#4338,#3501,#3502);
#3097=AXIS2_PLACEMENT_3D('',#4340,#3503,#3504);
#3098=AXIS2_PLACEMENT_3D('',#4342,#3506,#3507);
#3099=AXIS2_PLACEMENT_3D('',#4349,#3511,#3512);
#3100=AXIS2_PLACEMENT_3D('',#4353,#3515,#3516);
#3101=AXIS2_PLACEMENT_3D('',#4357,#3519,#3520);
#3102=AXIS2_PLACEMENT_3D('',#4361,#3523,#3524);
#3103=AXIS2_PLACEMENT_3D('',#4365,#3527,#3528);
#3104=AXIS2_PLACEMENT_3D('',#4367,#3530,#3531);
#3105=AXIS2_PLACEMENT_3D('',#4370,#3534,#3535);
#3106=AXIS2_PLACEMENT_3D('',#4372,#3537,#3538);
#3107=AXIS2_PLACEMENT_3D('',#4374,#3540,#3541);
#3108=AXIS2_PLACEMENT_3D('',#4376,#3543,#3544);
#3109=AXIS2_PLACEMENT_3D('',#4378,#3546,#3547);
#3110=AXIS2_PLACEMENT_3D('',#4379,#3548,#3549);
#3111=AXIS2_PLACEMENT_3D('',#4382,#3551,#3552);
#3112=AXIS2_PLACEMENT_3D('',#4383,#3553,#3554);
#3113=AXIS2_PLACEMENT_3D('',#4384,#3555,#3556);
#3476=DIRECTION('axis',(0.,0.,1.));
#3477=DIRECTION('refdir',(1.,0.,0.));
#3478=DIRECTION('center_axis',(0.,0.,1.));
#3479=DIRECTION('ref_axis',(-1.,0.,0.));
#3480=DIRECTION('center_axis',(-1.06387651071382E-15,0.,1.));
#3481=DIRECTION('ref_axis',(-1.,0.,-1.06387651071382E-15));
#3482=DIRECTION('',(-0.73423251512767,-8.99175499481012E-17,-0.678898087881602));
#3483=DIRECTION('center_axis',(1.06387651071382E-15,0.,-1.));
#3484=DIRECTION('ref_axis',(-1.,0.,-1.06387651071382E-15));
#3485=DIRECTION('center_axis',(1.06387651071382E-15,0.,-1.));
#3486=DIRECTION('ref_axis',(-1.,0.,-1.05179023385541E-15));
#3487=DIRECTION('center_axis',(-1.06387651071382E-15,0.,1.));
#3488=DIRECTION('ref_axis',(1.,0.,1.06387651071382E-15));
#3489=DIRECTION('center_axis',(-1.22464679914735E-16,-1.,-1.30287296353373E-31));
#3490=DIRECTION('ref_axis',(1.,-1.22464679914735E-16,1.02257383847054E-15));
#3491=DIRECTION('center_axis',(1.06387651071382E-15,0.,-1.));
#3492=DIRECTION('ref_axis',(1.,0.,1.06387651071382E-15));
#3493=DIRECTION('center_axis',(-1.06387651071382E-15,0.,1.));
#3494=DIRECTION('ref_axis',(1.,0.,1.06387651071382E-15));
#3495=DIRECTION('',(-0.866025403784439,-0.5,-9.21344084767719E-16));
#3496=DIRECTION('',(-0.866025403784439,0.5,-9.21344084767719E-16));
#3497=DIRECTION('',(6.40987562127854E-16,1.,6.81931611007542E-31));
#3498=DIRECTION('',(0.866025403784439,0.5,9.21344084767719E-16));
#3499=DIRECTION('',(0.866025403784439,-0.5,9.21344084767719E-16));
#3500=DIRECTION('',(-1.60246890531964E-16,-1.,-1.70482902751885E-31));
#3501=DIRECTION('center_axis',(1.06387651071382E-15,0.,-1.));
#3502=DIRECTION('ref_axis',(-1.,0.,-1.06387651071382E-15));
#3503=DIRECTION('center_axis',(1.06387651071382E-15,0.,-1.));
#3504=DIRECTION('ref_axis',(1.,0.,1.06387651071382E-15));
#3505=DIRECTION('',(-1.06387651071382E-15,0.,1.));
#3506=DIRECTION('center_axis',(0.0435778713738291,-0.0754790873051733,-0.996194698091746));
#3507=DIRECTION('ref_axis',(-0.866025403784439,-0.5,-3.35810244624808E-17));
#3508=DIRECTION('',(0.,0.997141949694316,-0.0755508581011305));
#3509=DIRECTION('',(-0.866025403784439,-0.5,0.));
#3510=DIRECTION('',(-0.863550259614423,0.498570974847158,-0.0755508581011305));
#3511=DIRECTION('center_axis',(0.0871557427476581,-1.3966436767316E-17,
-0.996194698091746));
#3512=DIRECTION('ref_axis',(-1.60246890531964E-16,-1.,1.77292017095641E-32));
#3513=DIRECTION('',(-1.60246890531964E-16,-1.,0.));
#3514=DIRECTION('',(-0.863550259614423,-0.498570974847158,-0.0755508581011305));
#3515=DIRECTION('center_axis',(0.0435778713738291,0.0754790873051733,-0.996194698091746));
#3516=DIRECTION('ref_axis',(0.866025403784439,-0.5,3.35810244624808E-17));
#3517=DIRECTION('',(0.866025403784439,-0.5,0.));
#3518=DIRECTION('',(-1.59381164582915E-16,-0.997141949694316,-0.0755508581011305));
#3519=DIRECTION('center_axis',(-0.0435778713738291,0.0754790873051733,-0.996194698091746));
#3520=DIRECTION('ref_axis',(0.866025403784439,0.5,-3.35810244624808E-17));
#3521=DIRECTION('',(0.866025403784439,0.5,0.));
#3522=DIRECTION('',(0.863550259614423,-0.498570974847159,-0.0755508581011305));
#3523=DIRECTION('center_axis',(-0.0871557427476581,5.58657470692638E-17,
-0.996194698091746));
#3524=DIRECTION('ref_axis',(6.40987562127854E-16,1.,4.7015367027096E-32));
#3525=DIRECTION('',(6.40987562127854E-16,1.,0.));
#3526=DIRECTION('',(0.863550259614423,0.498570974847158,-0.0755508581011305));
#3527=DIRECTION('center_axis',(-0.0435778713738291,-0.0754790873051733,
-0.996194698091746));
#3528=DIRECTION('ref_axis',(-0.866025403784439,0.5,3.35810244624808E-17));
#3529=DIRECTION('',(-0.866025403784439,0.5,0.));
#3530=DIRECTION('center_axis',(0.5,-0.866025403784439,0.));
#3531=DIRECTION('ref_axis',(-0.866025403784439,-0.5,0.));
#3532=DIRECTION('',(0.,0.,-1.));
#3533=DIRECTION('',(0.,0.,-1.));
#3534=DIRECTION('center_axis',(1.,-1.60246890531964E-16,0.));
#3535=DIRECTION('ref_axis',(-1.60246890531964E-16,-1.,0.));
#3536=DIRECTION('',(0.,0.,-1.));
#3537=DIRECTION('center_axis',(0.5,0.866025403784439,0.));
#3538=DIRECTION('ref_axis',(0.866025403784439,-0.5,0.));
#3539=DIRECTION('',(0.,0.,-1.));
#3540=DIRECTION('center_axis',(-0.5,0.866025403784439,0.));
#3541=DIRECTION('ref_axis',(0.866025403784439,0.5,0.));
#3542=DIRECTION('',(0.,0.,-1.));
#3543=DIRECTION('center_axis',(-1.,6.40987562127854E-16,0.));
#3544=DIRECTION('ref_axis',(6.40987562127854E-16,1.,0.));
#3545=DIRECTION('',(0.,0.,-1.));
#3546=DIRECTION('center_axis',(-0.5,-0.866025403784439,0.));
#3547=DIRECTION('ref_axis',(-0.866025403784439,0.5,0.));
#3548=DIRECTION('center_axis',(1.06387651071382E-15,0.,-1.));
#3549=DIRECTION('ref_axis',(-1.,0.,-1.06387651071382E-15));
#3550=DIRECTION('',(-1.06387651071382E-15,0.,1.));
#3551=DIRECTION('center_axis',(-1.06387651071382E-15,0.,1.));
#3552=DIRECTION('ref_axis',(-1.,0.,-1.06387651071382E-15));
#3553=DIRECTION('center_axis',(1.06387651071382E-15,0.,-1.));
#3554=DIRECTION('ref_axis',(-1.,0.,-1.06387651071382E-15));
#3555=DIRECTION('center_axis',(1.06387651071382E-15,0.,-1.));
#3556=DIRECTION('ref_axis',(-1.,0.,-1.06387651071382E-15));
#4312=CARTESIAN_POINT('',(0.,0.,0.));
#4313=CARTESIAN_POINT('Origin',(0.,0.,-4.87731));
#4314=CARTESIAN_POINT('',(0.966750000000005,1.1839272930757E-16,-4.80385688672847));
#4315=CARTESIAN_POINT('Origin',(5.11071050262126E-15,0.,-4.80385688672847));
#4316=CARTESIAN_POINT('',(0.754619999999998,-9.24142967572573E-17,-5.));
#4317=CARTESIAN_POINT('',(0.887310000000001,1.08664135135144E-16,-4.87731));
#4318=CARTESIAN_POINT('Origin',(0.,0.,-5.));
#4319=CARTESIAN_POINT('Origin',(-1.91497771928438E-15,0.,1.79999999999952));
#4320=CARTESIAN_POINT('',(1.89999999999999,-2.32682891837997E-16,1.79999999999953));
#4321=CARTESIAN_POINT('Origin',(-1.91497771928438E-15,0.,1.79999999999952));
#4322=CARTESIAN_POINT('',(1.69999999999999,-2.0818995585505E-16,1.99999999999953));
#4323=CARTESIAN_POINT('Origin',(1.7,-2.0818995585505E-16,1.79999999999952));
#4324=CARTESIAN_POINT('Origin',(-2.12775302142714E-15,0.,1.99999999999952));
#4325=CARTESIAN_POINT('Origin',(-1.9,0.,1.99999999999952));
#4326=CARTESIAN_POINT('',(0.75,-0.433012701892219,2.));
#4327=CARTESIAN_POINT('',(1.38777878078145E-16,-0.866025403784439,2.));
#4328=CARTESIAN_POINT('',(-0.149999999999999,-0.952627944162883,1.99999999999952));
#4329=CARTESIAN_POINT('',(-0.750000000000001,-0.433012701892219,2.));
#4330=CARTESIAN_POINT('',(-0.899999999999999,-0.346410161513776,1.99999999999952));
#4331=CARTESIAN_POINT('',(-0.75,0.43301270189222,2.));
#4332=CARTESIAN_POINT('',(-0.75,-0.21650635094611,1.99999999999952));
#4333=CARTESIAN_POINT('',(1.73472347597681E-17,0.866025403784439,2.));
#4334=CARTESIAN_POINT('',(-1.275,0.129903810567666,1.99999999999952));
#4335=CARTESIAN_POINT('',(0.75,0.433012701892219,2.));
#4336=CARTESIAN_POINT('',(-0.524999999999999,1.16913429510899,1.99999999999952));
#4337=CARTESIAN_POINT('',(0.75,0.216506350946109,1.99999999999952));
#4338=CARTESIAN_POINT('Origin',(-1.06387651071333E-15,0.,0.999999999999538));
#4339=CARTESIAN_POINT('',(1.9,-2.32682891837997E-16,-4.47419878923938E-13));
#4340=CARTESIAN_POINT('Origin',(4.74691816123085E-28,0.,-4.48558184615945E-13));
#4341=CARTESIAN_POINT('',(1.9,-2.32682891837997E-16,0.99999999999954));
#4342=CARTESIAN_POINT('Origin',(1.38777878078145E-16,-0.866025403784439,
1.));
#4343=CARTESIAN_POINT('',(1.38777878078145E-16,-0.866025403784439,1.));
#4344=CARTESIAN_POINT('',(0.,2.77555756156289E-16,0.934383502355557));
#4345=CARTESIAN_POINT('',(0.,-0.650754856401699,0.983689509218169));
#4346=CARTESIAN_POINT('',(0.75,-0.433012701892219,1.));
#4347=CARTESIAN_POINT('',(8.5846548499269E-17,-0.866025403784439,1.));
#4348=CARTESIAN_POINT('',(0.563570237279966,-0.325377428200849,0.983689509218169));
#4349=CARTESIAN_POINT('Origin',(0.75,-0.433012701892219,1.));
#4350=CARTESIAN_POINT('',(0.75,0.433012701892219,1.));
#4351=CARTESIAN_POINT('',(0.75,-0.433012701892219,1.));
#4352=CARTESIAN_POINT('',(0.563570237279966,0.32537742820085,0.983689509218169));
#4353=CARTESIAN_POINT('Origin',(0.75,0.433012701892219,1.));
#4354=CARTESIAN_POINT('',(0.,0.866025403784439,1.));
#4355=CARTESIAN_POINT('',(0.75,0.433012701892219,1.));
#4356=CARTESIAN_POINT('',(0.,0.650754856401699,0.983689509218169));
#4357=CARTESIAN_POINT('Origin',(0.,0.866025403784439,1.));
#4358=CARTESIAN_POINT('',(-0.75,0.43301270189222,1.));
#4359=CARTESIAN_POINT('',(1.73472347597681E-17,0.866025403784439,1.));
#4360=CARTESIAN_POINT('',(-0.563570237279966,0.325377428200849,0.983689509218169));
#4361=CARTESIAN_POINT('Origin',(-0.75,0.43301270189222,1.));
#4362=CARTESIAN_POINT('',(-0.750000000000001,-0.433012701892219,1.));
#4363=CARTESIAN_POINT('',(-0.75,0.43301270189222,1.));
#4364=CARTESIAN_POINT('',(-0.563570237279966,-0.325377428200849,0.983689509218169));
#4365=CARTESIAN_POINT('Origin',(-0.750000000000001,-0.433012701892219,1.));
#4366=CARTESIAN_POINT('',(-0.750000000000001,-0.433012701892219,1.));
#4367=CARTESIAN_POINT('Origin',(0.75,-0.433012701892219,2.));
#4368=CARTESIAN_POINT('',(0.75,-0.433012701892219,2.));
#4369=CARTESIAN_POINT('',(1.38777878078145E-16,-0.866025403784439,2.));
#4370=CARTESIAN_POINT('Origin',(0.75,0.433012701892219,2.));
#4371=CARTESIAN_POINT('',(0.75,0.433012701892219,2.));
#4372=CARTESIAN_POINT('Origin',(0.,0.866025403784439,2.));
#4373=CARTESIAN_POINT('',(1.73472347597681E-17,0.866025403784439,2.));
#4374=CARTESIAN_POINT('Origin',(-0.75,0.43301270189222,2.));
#4375=CARTESIAN_POINT('',(-0.75,0.43301270189222,2.));
#4376=CARTESIAN_POINT('Origin',(-0.750000000000001,-0.433012701892219,2.));
#4377=CARTESIAN_POINT('',(-0.750000000000001,-0.433012701892219,2.));
#4378=CARTESIAN_POINT('Origin',(1.38777878078145E-16,-0.866025403784439,
2.));
#4379=CARTESIAN_POINT('Origin',(2.65969127678468E-15,0.,-2.50000000000012));
#4380=CARTESIAN_POINT('',(0.96675,1.1839272930757E-16,-2.35150733091162E-13));
#4381=CARTESIAN_POINT('',(0.966750000000003,-1.1839272930757E-16,-2.50000000000012));
#4382=CARTESIAN_POINT('Origin',(2.48491185144619E-28,0.,-2.35922392732846E-13));
#4383=CARTESIAN_POINT('Origin',(5.27355936696949E-15,0.,-5.));
#4384=CARTESIAN_POINT('Origin',(-0.999999999999996,0.,-2.37147131571737E-13));
#4974=UNCERTAINTY_MEASURE_WITH_UNIT(LENGTH_MEASURE(0.01),#4995,
'DISTANCE_ACCURACY_VALUE',
'Maximum model space distance between geometric entities at asserted c
onnectivities');
#4982=UNCERTAINTY_MEASURE_WITH_UNIT(LENGTH_MEASURE(0.01),#4995,
'DISTANCE_ACCURACY_VALUE',
'Maximum model space distance between geometric entities at asserted c
onnectivities');
#4986=(
GEOMETRIC_REPRESENTATION_CONTEXT(3)
GLOBAL_UNCERTAINTY_ASSIGNED_CONTEXT((#4974))
GLOBAL_UNIT_ASSIGNED_CONTEXT((#4995,#4997,#4998))
REPRESENTATION_CONTEXT('','3D')
);
#4994=(
GEOMETRIC_REPRESENTATION_CONTEXT(3)
GLOBAL_UNCERTAINTY_ASSIGNED_CONTEXT((#4982))
GLOBAL_UNIT_ASSIGNED_CONTEXT((#4995,#4997,#4998))
REPRESENTATION_CONTEXT('','3D')
);
#4995=(
LENGTH_UNIT()
NAMED_UNIT(*)
SI_UNIT(.MILLI.,.METRE.)
);
#4997=(
NAMED_UNIT(*)
PLANE_ANGLE_UNIT()
SI_UNIT($,.RADIAN.)
);
#4998=(
NAMED_UNIT(*)
SI_UNIT($,.STERADIAN.)
SOLID_ANGLE_UNIT()
);
#5002=SHAPE_DEFINITION_REPRESENTATION(#5013,#5034);
#5013=PRODUCT_DEFINITION_SHAPE('',$,#5046);
#5034=SHAPE_REPRESENTATION('',(#3087),#4986);
#5042=PRODUCT_DEFINITION_CONTEXT('part definition',#5077,'design');
#5046=PRODUCT_DEFINITION(
'BSHCS ASME B18.3.1M - M2x0.4 x 5 Steel Grade 2 Plain_2','Screw_03',#5057,
#5042);
#5057=PRODUCT_DEFINITION_FORMATION('',$,#5082);
#5077=APPLICATION_CONTEXT(
'Core Data for Automotive Mechanical Design Process');
#5078=PRODUCT_CONTEXT('part definition',#5077,'mechanical');
#5082=PRODUCT('BSHCS ASME B18.3.1M - M2x0.4 x 5 Steel Grade 2 Plain_2',
'Screw_03',
'Broached Hexagon Socket Head Cap Screw ASME B18.3.1M - M2x0.4 x 5',(#5078));
#5091=PRESENTATION_STYLE_ASSIGNMENT((#5096));
#5096=SURFACE_STYLE_USAGE(.BOTH.,#5101);
#5101=SURFACE_SIDE_STYLE('',(#5106));
#5106=SURFACE_STYLE_FILL_AREA(#5111);
#5111=FILL_AREA_STYLE('Opaque(160,160,160)',(#5116));
#5116=FILL_AREA_STYLE_COLOUR('Opaque(160,160,160)',#5121);
#5121=COLOUR_RGB('Opaque(160,160,160)', 0.09019608, 0.27058824, 0.51372549);
ENDSEC;
END-ISO-10303-21;
